ISO-10303-21;
HEADER;
FILE_DESCRIPTION (('STEP AP203'),
    '1' );
FILE_NAME ('F2.step',
    '2026-10-31T14:11:27',
    ( '' ),
    ( '' ),
    'SwSTEP 2.0',
    'SolidWorks 2024',
    '' );
FILE_SCHEMA (( 'AUTOMOTIVE_DESIGN' ));
ENDSEC;

DATA;
#33=EDGE_CURVE ( 'NONE', #13752, #1171, #21401, .T. ) ;
#43=CARTESIAN_POINT ( 'NONE',  ( 0.000000000000000000, 0.000000000000000000, -5.000000000000000000 ) ) ;
#49=ADVANCED_FACE ( 'NONE', ( #3230, #23291, #10261, #6805 ), #6927, .T. ) ;
#84=CARTESIAN_POINT ( 'NONE',  ( 5.000000000000000000, -29.85000000000000142, -12.00000000000000000 ) ) ;
#122=CIRCLE ( 'NONE', #15304, 1.250000000000000222 ) ;
#125=EDGE_CURVE ( 'NONE', #15552, #9993, #3113, .T. ) ;
#164=CARTESIAN_POINT ( 'NONE',  ( 0.000000000000000000, -17.30000000000000071, -2.500000000000000000 ) ) ;
#173=ORIENTED_EDGE ( 'NONE', *, *, #19680, .T. ) ;
#195=CARTESIAN_POINT ( 'NONE',  ( -27.00000000000000000, -27.34999999999999787, -2.500000000000000000 ) ) ;
#212=ORIENTED_EDGE ( 'NONE', *, *, #11041, .T. ) ;
#255=VERTEX_POINT ( 'NONE', #3589 ) ;
#266=VECTOR ( 'NONE', #19546, 1000.000000000000000 ) ;
#267=AXIS2_PLACEMENT_3D ( 'NONE', #2294, #14886, #3727 ) ;
#275=DIRECTION ( 'NONE',  ( -1.000000000000000000, 0.000000000000000000, 0.000000000000000000 ) ) ;
#277=CARTESIAN_POINT ( 'NONE',  ( 2.500000000000000000, -30.47499999999999787, -21.50000000000000000 ) ) ;
#288=CARTESIAN_POINT ( 'NONE',  ( 2.500000000000000000, -28.60000000000000142, -19.00000000000000000 ) ) ;
#377=ORIENTED_EDGE ( 'NONE', *, *, #9879, .T. ) ;
#397=DIRECTION ( 'NONE',  ( 1.000000000000000000, 1.829748171496159792E-16, 1.829748171496159792E-16 ) ) ;
#405=DIRECTION ( 'NONE',  ( 0.000000000000000000, 1.000000000000000000, 0.000000000000000000 ) ) ;
#415=DIRECTION ( 'NONE',  ( 1.000000000000000000, 0.000000000000000000, 0.000000000000000000 ) ) ;
#418=VERTEX_POINT ( 'NONE', #20437 ) ;
#433=ORIENTED_EDGE ( 'NONE', *, *, #10660, .T. ) ;
#520=DIRECTION ( 'NONE',  ( 0.000000000000000000, 0.000000000000000000, 1.000000000000000000 ) ) ;
#528=CARTESIAN_POINT ( 'NONE',  ( 5.000000000000000000, -31.09999999999999787, -6.250000000000000000 ) ) ;
#539=CARTESIAN_POINT ( 'NONE',  ( 6.500000000000000000, -17.30000000000000071, -2.500000000000000000 ) ) ;
#544=VERTEX_POINT ( 'NONE', #12446 ) ;
#560=VERTEX_POINT ( 'NONE', #19918 ) ;
#577=VERTEX_POINT ( 'NONE', #21676 ) ;
#581=AXIS2_PLACEMENT_3D ( 'NONE', #2091, #6128, #20273 ) ;
#605=CARTESIAN_POINT ( 'NONE',  ( -27.00000000000000000, -28.60000000000000142, -2.500000000000000000 ) ) ;
#637=ORIENTED_EDGE ( 'NONE', *, *, #4722, .T. ) ;
#641=VECTOR ( 'NONE', #20224, 1000.000000000000000 ) ;
#728=CARTESIAN_POINT ( 'NONE',  ( -27.00000000000000000, -31.09999999999999787, -6.250000000000000000 ) ) ;
#746=VERTEX_POINT ( 'NONE', #11500 ) ;
#792=EDGE_CURVE ( 'NONE', #13752, #6915, #20618, .T. ) ;
#816=EDGE_CURVE ( 'NONE', #8039, #560, #11774, .T. ) ;
#958=ORIENTED_EDGE ( 'NONE', *, *, #5201, .T. ) ;
#978=CARTESIAN_POINT ( 'NONE',  ( -27.00000000000000000, -28.60000000000000142, -19.00000000000000000 ) ) ;
#1018=ORIENTED_EDGE ( 'NONE', *, *, #18119, .T. ) ;
#1023=CIRCLE ( 'NONE', #4074, 6.500000000000000000 ) ;
#1084=EDGE_CURVE ( 'NONE', #544, #15192, #15963, .T. ) ;
#1095=CARTESIAN_POINT ( 'NONE',  ( 5.000000000000000000, -28.60000000000000142, -19.00000000000000000 ) ) ;
#1099=CARTESIAN_POINT ( 'NONE',  ( -23.50000000000000000, -20.00000000000000000, -2.500000000000000000 ) ) ;
#1108=CYLINDRICAL_SURFACE ( 'NONE', #17422, 6.500000000000000000 ) ;
#1113=CARTESIAN_POINT ( 'NONE',  ( -27.00000000000000000, -29.85000000000000142, -12.00000000000000000 ) ) ;
#1171=VERTEX_POINT ( 'NONE', #18349 ) ;
#1182=DIRECTION ( 'NONE',  ( 0.8846153846154072298, -0.4663213712685009837, 0.000000000000000000 ) ) ;
#1221=DIRECTION ( 'NONE',  ( 0.000000000000000000, 0.000000000000000000, -1.000000000000000000 ) ) ;
#1235=CIRCLE ( 'NONE', #5788, 2.500000000000001332 ) ;
#1238=LINE ( 'NONE', #8512, #13178 ) ;
#1239=EDGE_CURVE ( 'NONE', #5066, #2028, #1023, .T. ) ;
#1322=DIRECTION ( 'NONE',  ( 0.000000000000000000, -1.000000000000000000, 0.000000000000000000 ) ) ;
#1399=CARTESIAN_POINT ( 'NONE',  ( -24.50000000000000000, -30.47499999999999787, -21.50000000000000000 ) ) ;
#1461=DIRECTION ( 'NONE',  ( 0.000000000000000000, 0.000000000000000000, -1.000000000000000000 ) ) ;
#1490=ORIENTED_EDGE ( 'NONE', *, *, #5146, .F. ) ;
#1506=LINE ( 'NONE', #8425, #5948 ) ;
#1513=ORIENTED_EDGE ( 'NONE', *, *, #33, .F. ) ;
#1519=CARTESIAN_POINT ( 'NONE',  ( 5.000000000000000000, -30.47499999999999787, -19.00000000000000000 ) ) ;
#1542=CARTESIAN_POINT ( 'NONE',  ( -24.50000000000000000, -31.09999999999999787, -19.00000000000000000 ) ) ;
#1557=CARTESIAN_POINT ( 'NONE',  ( 5.000000000000000000, -31.09999999999999787, -2.500000000000000000 ) ) ;
#1597=DIRECTION ( 'NONE',  ( -1.000000000000000000, 0.000000000000000000, 0.000000000000000000 ) ) ;
#1630=DIRECTION ( 'NONE',  ( 0.000000000000000000, 1.000000000000000000, 0.000000000000000000 ) ) ;
#1651=ADVANCED_FACE ( 'NONE', ( #16170 ), #12629, .T. ) ;
#1709=MECHANICAL_CONTEXT ( 'NONE', #7460, 'mechanical' ) ;
#1744=CARTESIAN_POINT ( 'NONE',  ( 0.000000000000000000, 0.000000000000000000, -2.500000000000000000 ) ) ;
#1754=CARTESIAN_POINT ( 'NONE',  ( -23.50000000000000000, -20.00000000000000000, -2.500000000000000000 ) ) ;
#1809=UNCERTAINTY_MEASURE_WITH_UNIT (LENGTH_MEASURE( 1.000000000000000082E-05 ), #16931, 'distance_accuracy_value', 'NONE');
#1830=LINE ( 'NONE', #14662, #10546 ) ;
#1845=DIRECTION ( 'NONE',  ( 0.000000000000000000, -1.000000000000000000, 0.000000000000000000 ) ) ;
#1853=LINE ( 'NONE', #7565, #21750 ) ;
#1859=DIRECTION ( 'NONE',  ( 0.000000000000000000, 0.000000000000000000, -1.000000000000000000 ) ) ;
#1862=ORIENTED_EDGE ( 'NONE', *, *, #4041, .F. ) ;
#1902=AXIS2_PLACEMENT_3D ( 'NONE', #1557, #14166, #21405 ) ;
#1953=DIRECTION ( 'NONE',  ( 0.000000000000000000, 0.000000000000000000, -1.000000000000000000 ) ) ;
#1965=DIRECTION ( 'NONE',  ( 0.000000000000000000, 0.000000000000000000, -1.000000000000000000 ) ) ;
#1973=DIRECTION ( 'NONE',  ( -1.000000000000000000, 0.000000000000000000, 0.000000000000000000 ) ) ;
#2026=SHAPE_REPRESENTATION ( 'F2', ( #12739 ), #2093 ) ;
#2028=VERTEX_POINT ( 'NONE', #21590 ) ;
#2069=CARTESIAN_POINT ( 'NONE',  ( 5.000000000000000000, -28.60000000000000142, -21.50000000000000000 ) ) ;
#2091=CARTESIAN_POINT ( 'NONE',  ( 2.500000000000000000, -31.09999999999999787, -19.00000000000000000 ) ) ;
#2093=( GEOMETRIC_REPRESENTATION_CONTEXT ( 3 ) GLOBAL_UNCERTAINTY_ASSIGNED_CONTEXT ( ( #1809 ) ) GLOBAL_UNIT_ASSIGNED_CONTEXT ( ( #16931, #22154, #17045 ) ) REPRESENTATION_CONTEXT ( 'NONE', 'WORKASPACE' ) );
#2097=EDGE_CURVE ( 'NONE', #15533, #4748, #9740, .T. ) ;
#2123=CIRCLE ( 'NONE', #4795, 2.500000000000000000 ) ;
#2159=LINE ( 'NONE', #605, #5577 ) ;
#2162=CYLINDRICAL_SURFACE ( 'NONE', #2377, 3.499999999999999556 ) ;
#2200=VERTEX_POINT ( 'NONE', #21828 ) ;
#2294=CARTESIAN_POINT ( 'NONE',  ( -11.00000000000000000, -27.34999999999999787, -6.250000000000000000 ) ) ;
#2351=ORIENTED_EDGE ( 'NONE', *, *, #20302, .T. ) ;
#2375=VERTEX_POINT ( 'NONE', #23445 ) ;
#2377=AXIS2_PLACEMENT_3D ( 'NONE', #17122, #16763, #22218 ) ;
#2510=AXIS2_PLACEMENT_3D ( 'NONE', #8914, #7022, #19484 ) ;
#2559=DIRECTION ( 'NONE',  ( 0.000000000000000000, 1.000000000000000000, 0.000000000000000000 ) ) ;
#2569=CARTESIAN_POINT ( 'NONE',  ( 0.000000000000000000, 0.000000000000000000, 0.000000000000000000 ) ) ;
#2614=ORIENTED_EDGE ( 'NONE', *, *, #15857, .F. ) ;
#2660=CARTESIAN_POINT ( 'NONE',  ( -27.00000000000000000, -31.09999999999999787, -21.50000000000000000 ) ) ;
#2665=ADVANCED_FACE ( 'NONE', ( #20827 ), #6455, .T. ) ;
#2690=ORIENTED_EDGE ( 'NONE', *, *, #20301, .T. ) ;
#2709=VECTOR ( 'NONE', #13240, 1000.000000000000000 ) ;
#2726=ORIENTED_EDGE ( 'NONE', *, *, #8209, .F. ) ;
#2733=DIRECTION ( 'NONE',  ( 0.000000000000000000, 0.000000000000000000, 1.000000000000000000 ) ) ;
#2868=CARTESIAN_POINT ( 'NONE',  ( -20.00000000000000000, -20.00000000000000000, -5.000000000000000000 ) ) ;
#2902=CARTESIAN_POINT ( 'NONE',  ( 2.500000000000000000, 3.061616997868383141E-16, -2.500000000000000000 ) ) ;
#2915=AXIS2_PLACEMENT_3D ( 'NONE', #6264, #15282, #20739 ) ;
#2917=VECTOR ( 'NONE', #21359, 999.9999999999998863 ) ;
#2992=CARTESIAN_POINT ( 'NONE',  ( 6.500000000000000000, -17.30000000000000071, -2.500000000000000000 ) ) ;
#3064=ORIENTED_EDGE ( 'NONE', *, *, #3188, .F. ) ;
#3113=LINE ( 'NONE', #14266, #3477 ) ;
#3122=VECTOR ( 'NONE', #19411, 1000.000000000000000 ) ;
#3151=VECTOR ( 'NONE', #21306, 1000.000000000000000 ) ;
#3170=CARTESIAN_POINT ( 'NONE',  ( 2.500000000000000000, -28.60000000000000142, -19.00000000000000000 ) ) ;
#3188=EDGE_CURVE ( 'NONE', #7380, #20922, #12577, .T. ) ;
#3216=DIRECTION ( 'NONE',  ( 0.7071067811865475727, 0.000000000000000000, -0.7071067811865474617 ) ) ;
#3224=DIRECTION ( 'NONE',  ( 0.000000000000000000, 0.000000000000000000, 1.000000000000000000 ) ) ;
#3230=FACE_OUTER_BOUND ( 'NONE', #7963, .T. ) ;
#3238=EDGE_CURVE ( 'NONE', #20234, #8857, #1506, .T. ) ;
#3266=ADVANCED_FACE ( 'NONE', ( #14113, #12463, #19692, #22903 ), #23356, .F. ) ;
#3324=ADVANCED_FACE ( 'NONE', ( #9473 ), #9351, .F. ) ;
#3370=EDGE_LOOP ( 'NONE', ( #21626, #22225 ) ) ;
#3377=CARTESIAN_POINT ( 'NONE',  ( -20.00000000000000000, -20.00000000000000000, -2.500000000000000000 ) ) ;
#3430=CARTESIAN_POINT ( 'NONE',  ( 6.500000000000000000, -17.30000000000000071, -5.000000000000000000 ) ) ;
#3443=DIRECTION ( 'NONE',  ( -1.000000000000000000, 0.000000000000000000, 0.000000000000000000 ) ) ;
#3449=CYLINDRICAL_SURFACE ( 'NONE', #17209, 6.499999999999997335 ) ;
#3475=VECTOR ( 'NONE', #1630, 1000.000000000000000 ) ;
#3477=VECTOR ( 'NONE', #7159, 1000.000000000000000 ) ;
#3503=CARTESIAN_POINT ( 'NONE',  ( 5.000000000000000000, -31.09999999999999787, -21.50000000000000000 ) ) ;
#3514=AXIS2_PLACEMENT_3D ( 'NONE', #1542, #8811, #14617 ) ;
#3576=ORIENTED_EDGE ( 'NONE', *, *, #10562, .F. ) ;
#3589=CARTESIAN_POINT ( 'NONE',  ( -27.00000000000000000, -28.60000000000000142, -6.250000000000000000 ) ) ;
#3609=CARTESIAN_POINT ( 'NONE',  ( 11.50000000000000000, -23.36217782649110219, -2.500000000000000000 ) ) ;
#3635=VERTEX_POINT ( 'NONE', #12335 ) ;
#3676=EDGE_CURVE ( 'NONE', #2375, #20234, #21688, .T. ) ;
#3727=DIRECTION ( 'NONE',  ( 0.000000000000000000, 0.000000000000000000, 1.000000000000000000 ) ) ;
#3764=FACE_OUTER_BOUND ( 'NONE', #16610, .T. ) ;
#3765=EDGE_LOOP ( 'NONE', ( #7917, #14287, #16393, #6412 ) ) ;
#3892=FACE_OUTER_BOUND ( 'NONE', #10247, .T. ) ;
#3933=DIRECTION ( 'NONE',  ( -0.7071067811865475727, 0.000000000000000000, -0.7071067811865475727 ) ) ;
#3992=ADVANCED_FACE ( 'NONE', ( #4096 ), #10056, .T. ) ;
#4011=DIRECTION ( 'NONE',  ( 2.269881297312570136E-47, 1.000000000000000000, -2.269881297312570136E-47 ) ) ;
#4029=ORIENTED_EDGE ( 'NONE', *, *, #816, .F. ) ;
#4041=EDGE_CURVE ( 'NONE', #20805, #8421, #13129, .T. ) ;
#4074=AXIS2_PLACEMENT_3D ( 'NONE', #18580, #19996, #16783 ) ;
#4075=EDGE_LOOP ( 'NONE', ( #5321, #7486, #5780, #19354 ) ) ;
#4096=FACE_OUTER_BOUND ( 'NONE', #6552, .T. ) ;
#4101=AXIS2_PLACEMENT_3D ( 'NONE', #19515, #16629, #20560 ) ;
#4116=CARTESIAN_POINT ( 'NONE',  ( 0.000000000000000000, -17.30000000000000071, -5.000000000000000000 ) ) ;
#4123=ORIENTED_EDGE ( 'NONE', *, *, #1084, .F. ) ;
#4199=AXIS2_PLACEMENT_3D ( 'NONE', #2868, #14933, #3443 ) ;
#4345=ORIENTED_EDGE ( 'NONE', *, *, #20302, .F. ) ;
#4364=EDGE_LOOP ( 'NONE', ( #7729, #20577 ) ) ;
#4409=DIRECTION ( 'NONE',  ( -0.6944962871189666043, 0.7194962871189606313, 0.000000000000000000 ) ) ;
#4430=ORIENTED_EDGE ( 'NONE', *, *, #10660, .F. ) ;
#4440=CIRCLE ( 'NONE', #2915, 6.500000000000000888 ) ;
#4495=ORIENTED_EDGE ( 'NONE', *, *, #2097, .F. ) ;
#4522=EDGE_LOOP ( 'NONE', ( #16197, #13682, #20196, #637 ) ) ;
#4606=DIRECTION ( 'NONE',  ( -0.6944962871189167553, 0.7194962871190087039, 0.000000000000000000 ) ) ;
#4657=CIRCLE ( 'NONE', #10373, 2.500000000000001332 ) ;
#4666=LINE ( 'NONE', #6571, #12290 ) ;
#4709=ORIENTED_EDGE ( 'NONE', *, *, #21465, .T. ) ;
#4722=EDGE_CURVE ( 'NONE', #21863, #16294, #6165, .T. ) ;
#4746=ORIENTED_EDGE ( 'NONE', *, *, #19575, .T. ) ;
#4748=VERTEX_POINT ( 'NONE', #23044 ) ;
#4750=EDGE_CURVE ( 'NONE', #20922, #544, #5035, .T. ) ;
#4774=EDGE_CURVE ( 'NONE', #418, #560, #11070, .T. ) ;
#4795=AXIS2_PLACEMENT_3D ( 'NONE', #11034, #1859, #5791 ) ;
#4891=ORIENTED_EDGE ( 'NONE', *, *, #20493, .F. ) ;
#4898=DIRECTION ( 'NONE',  ( 0.000000000000000000, 1.000000000000000000, 0.000000000000000000 ) ) ;
#4905=AXIS2_PLACEMENT_3D ( 'NONE', #6717, #13948, #21184 ) ;
#5014=DIRECTION ( 'NONE',  ( 1.000000000000000000, 0.000000000000000000, 1.480297366166879989E-16 ) ) ;
#5035=CIRCLE ( 'NONE', #23207, 7.000000000000004441 ) ;
#5045=ORIENTED_EDGE ( 'NONE', *, *, #22019, .T. ) ;
#5052=LINE ( 'NONE', #22964, #3151 ) ;
#5055=VECTOR ( 'NONE', #2559, 1000.000000000000000 ) ;
#5066=VERTEX_POINT ( 'NONE', #11426 ) ;
#5138=EDGE_CURVE ( 'NONE', #418, #13752, #11777, .T. ) ;
#5146=EDGE_CURVE ( 'NONE', #18183, #22408, #19235, .T. ) ;
#5162=CARTESIAN_POINT ( 'NONE',  ( -23.50000000000000000, -20.00000000000000000, -5.000000000000000000 ) ) ;
#5201=EDGE_CURVE ( 'NONE', #9993, #577, #17071, .T. ) ;
#5217=VECTOR ( 'NONE', #1597, 1000.000000000000000 ) ;
#5241=ORIENTED_EDGE ( 'NONE', *, *, #16937, .F. ) ;
#5269=CARTESIAN_POINT ( 'NONE',  ( -27.00000000000000000, -20.00000000000000000, -2.500000000000000000 ) ) ;
#5279=LINE ( 'NONE', #2069, #5217 ) ;
#5321=ORIENTED_EDGE ( 'NONE', *, *, #21465, .F. ) ;
#5364=CARTESIAN_POINT ( 'NONE',  ( -2.500000000000000000, -17.30000000000000071, -5.000000000000000000 ) ) ;
#5387=EDGE_LOOP ( 'NONE', ( #15085, #6435, #1513, #16733 ) ) ;
#5394=AXIS2_PLACEMENT_3D ( 'NONE', #18396, #4011, #9127 ) ;
#5442=ORIENTED_EDGE ( 'NONE', *, *, #19017, .F. ) ;
#5513=SHAPE_DEFINITION_REPRESENTATION ( #6475, #2026 ) ;
#5577=VECTOR ( 'NONE', #15342, 1000.000000000000000 ) ;
#5632=CARTESIAN_POINT ( 'NONE',  ( -2.500000000000000000, 0.000000000000000000, -2.500000000000000000 ) ) ;
#5650=ADVANCED_FACE ( 'NONE', ( #17518 ), #1108, .T. ) ;
#5661=DIRECTION ( 'NONE',  ( 0.000000000000000000, 0.000000000000000000, 1.000000000000000000 ) ) ;
#5762=ORIENTED_EDGE ( 'NONE', *, *, #7026, .F. ) ;
#5774=CARTESIAN_POINT ( 'NONE',  ( -24.50000000000000000, -28.60000000000000142, -19.00000000000000000 ) ) ;
#5778=SHAPE_REPRESENTATION_RELATIONSHIP ( 'NONE' , 'NONE' ,  #2026, #21806 ) ;
#5780=ORIENTED_EDGE ( 'NONE', *, *, #23303, .F. ) ;
#5788=AXIS2_PLACEMENT_3D ( 'NONE', #288, #1845, #16332 ) ;
#5791=DIRECTION ( 'NONE',  ( -1.000000000000000000, 0.000000000000000000, 0.000000000000000000 ) ) ;
#5797=VECTOR ( 'NONE', #397, 1000.000000000000000 ) ;
#5799=ADVANCED_FACE ( 'NONE', ( #11963 ), #22962, .T. ) ;
#5807=EDGE_LOOP ( 'NONE', ( #16764, #9220, #11543, #16078 ) ) ;
#5862=ORIENTED_EDGE ( 'NONE', *, *, #3676, .T. ) ;
#5948=VECTOR ( 'NONE', #16007, 1000.000000000000000 ) ;
#5984=DIRECTION ( 'NONE',  ( -1.000000000000000000, 0.000000000000000000, 0.000000000000000000 ) ) ;
#6004=ADVANCED_FACE ( 'NONE', ( #14407 ), #19887, .F. ) ;
#6017=EDGE_CURVE ( 'NONE', #2028, #18242, #22119, .T. ) ;
#6128=DIRECTION ( 'NONE',  ( 0.000000000000000000, 1.000000000000000000, 0.000000000000000000 ) ) ;
#6165=CIRCLE ( 'NONE', #12258, 1.250000000000000222 ) ;
#6192=VECTOR ( 'NONE', #14657, 1000.000000000000000 ) ;
#6264=CARTESIAN_POINT ( 'NONE',  ( 11.50000000000000000, -23.36217782649110219, -2.500000000000000000 ) ) ;
#6276=CIRCLE ( 'NONE', #8943, 2.500000000000000000 ) ;
#6279=CARTESIAN_POINT ( 'NONE',  ( 0.000000000000000000, 0.000000000000000000, -2.500000000000000000 ) ) ;
#6286=EDGE_CURVE ( 'NONE', #11837, #255, #122, .T. ) ;
#6350=ORIENTED_EDGE ( 'NONE', *, *, #4750, .T. ) ;
#6382=ORIENTED_EDGE ( 'NONE', *, *, #23303, .T. ) ;
#6408=ORIENTED_EDGE ( 'NONE', *, *, #20418, .F. ) ;
#6409=DIRECTION ( 'NONE',  ( -0.7071067811865475727, 0.000000000000000000, -0.7071067811865475727 ) ) ;
#6412=ORIENTED_EDGE ( 'NONE', *, *, #4774, .T. ) ;
#6435=ORIENTED_EDGE ( 'NONE', *, *, #8520, .F. ) ;
#6453=ADVANCED_FACE ( 'NONE', ( #10966 ), #18185, .T. ) ;
#6455=PLANE ( 'NONE',  #17710 ) ;
#6475=PRODUCT_DEFINITION_SHAPE ( 'NONE', 'NONE',  #20819 ) ;
#6549=PLANE ( 'NONE',  #13986 ) ;
#6552=EDGE_LOOP ( 'NONE', ( #173, #4123, #18368, #22368 ) ) ;
#6555=DIRECTION ( 'NONE',  ( 2.269881297312570136E-47, 1.000000000000000000, -2.269881297312570136E-47 ) ) ;
#6571=CARTESIAN_POINT ( 'NONE',  ( -27.00000000000000000, -20.00000000000000000, -5.000000000000000000 ) ) ;
#6576=CIRCLE ( 'NONE', #19835, 2.500000000000000000 ) ;
#6608=ORIENTED_EDGE ( 'NONE', *, *, #14740, .F. ) ;
#6609=DIRECTION ( 'NONE',  ( 0.8846153846153640421, -0.4663213712685829182, 0.000000000000000000 ) ) ;
#6632=ORIENTED_EDGE ( 'NONE', *, *, #14216, .F. ) ;
#6660=CARTESIAN_POINT ( 'NONE',  ( -17.54011269262000283, -27.34999999999999787, -2.500000000000000000 ) ) ;
#6676=ORIENTED_EDGE ( 'NONE', *, *, #7975, .F. ) ;
#6688=ORIENTED_EDGE ( 'NONE', *, *, #13414, .F. ) ;
#6717=CARTESIAN_POINT ( 'NONE',  ( 5.000000000000000000, -28.60000000000000142, -21.50000000000000000 ) ) ;
#6766=LINE ( 'NONE', #21466, #3475 ) ;
#6799=CARTESIAN_POINT ( 'NONE',  ( 5.000000000000000000, -27.34999999999999787, -6.250000000000000000 ) ) ;
#6805=FACE_BOUND ( 'NONE', #4364, .T. ) ;
#6815=FACE_OUTER_BOUND ( 'NONE', #4075, .T. ) ;
#6828=VERTEX_POINT ( 'NONE', #1754 ) ;
#6915=VERTEX_POINT ( 'NONE', #3430 ) ;
#6917=VECTOR ( 'NONE', #1221, 1000.000000000000000 ) ;
#6920=ORIENTED_EDGE ( 'NONE', *, *, #15857, .T. ) ;
#6927=PLANE ( 'NONE',  #9562 ) ;
#6956=PRODUCT_DEFINITION_FORMATION_WITH_SPECIFIED_SOURCE ( 'ANY', '', #15182, .NOT_KNOWN. ) ;
#6957=ORIENTED_EDGE ( 'NONE', *, *, #33, .T. ) ;
#6970=ADVANCED_FACE ( 'NONE', ( #17930 ), #12705, .F. ) ;
#6973=AXIS2_PLACEMENT_3D ( 'NONE', #11355, #22235, #5984 ) ;
#6983=CIRCLE ( 'NONE', #18345, 7.000000000000004441 ) ;
#6986=ORIENTED_EDGE ( 'NONE', *, *, #20301, .F. ) ;
#7022=DIRECTION ( 'NONE',  ( 0.000000000000000000, 0.000000000000000000, -1.000000000000000000 ) ) ;
#7026=EDGE_CURVE ( 'NONE', #14214, #2200, #10585, .T. ) ;
#7047=DIRECTION ( 'NONE',  ( 0.000000000000000000, 0.000000000000000000, 1.000000000000000000 ) ) ;
#7087=LINE ( 'NONE', #5632, #19625 ) ;
#7117=CARTESIAN_POINT ( 'NONE',  ( 2.500000000000000000, -31.09999999999999787, -21.50000000000000000 ) ) ;
#7118=CARTESIAN_POINT ( 'NONE',  ( -8.080225385240000335, -15.72171916155420313, -5.000000000000000000 ) ) ;
#7153=ORIENTED_EDGE ( 'NONE', *, *, #9879, .F. ) ;
#7159=DIRECTION ( 'NONE',  ( -1.000000000000000000, 0.000000000000000000, 0.000000000000000000 ) ) ;
#7174=DIRECTION ( 'NONE',  ( 0.000000000000000000, 0.000000000000000000, 1.000000000000000000 ) ) ;
#7198=DIRECTION ( 'NONE',  ( -1.000000000000000000, 0.000000000000000000, 0.000000000000000000 ) ) ;
#7325=AXIS2_PLACEMENT_3D ( 'NONE', #21798, #7668, #405 ) ;
#7333=CARTESIAN_POINT ( 'NONE',  ( 4.267766952966368876, -28.60000000000000142, -20.76776695296636888 ) ) ;
#7352=DIRECTION ( 'NONE',  ( -1.000000000000000000, 0.000000000000000000, 0.000000000000000000 ) ) ;
#7380=VERTEX_POINT ( 'NONE', #18111 ) ;
#7412=EDGE_CURVE ( 'NONE', #2200, #8421, #10999, .T. ) ;
#7417=ORIENTED_EDGE ( 'NONE', *, *, #22161, .T. ) ;
#7431=DIRECTION ( 'NONE',  ( 0.000000000000000000, 0.000000000000000000, -1.000000000000000000 ) ) ;
#7459=VERTEX_POINT ( 'NONE', #5162 ) ;
#7460=APPLICATION_CONTEXT ( 'configuration controlled 3d designs of mechanical parts and assemblies' ) ;
#7479=CARTESIAN_POINT ( 'NONE',  ( -20.00000000000000000, -20.00000000000000000, -2.500000000000000000 ) ) ;
#7486=ORIENTED_EDGE ( 'NONE', *, *, #13985, .T. ) ;
#7556=CARTESIAN_POINT ( 'NONE',  ( 2.500000000000000000, -31.09999999999999787, -19.00000000000000000 ) ) ;
#7565=CARTESIAN_POINT ( 'NONE',  ( 6.500000000000000000, 0.000000000000000000, -2.500000000000000000 ) ) ;
#7641=EDGE_CURVE ( 'NONE', #18815, #15778, #19861, .T. ) ;
#7657=LINE ( 'NONE', #2660, #2709 ) ;
#7663=CARTESIAN_POINT ( 'NONE',  ( -2.500000000000000000, 0.000000000000000000, -2.500000000000000000 ) ) ;
#7668=DIRECTION ( 'NONE',  ( 1.000000000000000000, 0.000000000000000000, 0.000000000000000000 ) ) ;
#7729=ORIENTED_EDGE ( 'NONE', *, *, #7641, .T. ) ;
#7775=DIRECTION ( 'NONE',  ( 1.000000000000000000, -3.416070845000479880E-16, 0.000000000000000000 ) ) ;
#7863=ORIENTED_EDGE ( 'NONE', *, *, #14216, .T. ) ;
#7883=CARTESIAN_POINT ( 'NONE',  ( 5.000000000000000000, -27.34999999999999787, -2.500000000000000000 ) ) ;
#7917=ORIENTED_EDGE ( 'NONE', *, *, #13142, .T. ) ;
#7952=ORIENTED_EDGE ( 'NONE', *, *, #21702, .F. ) ;
#7959=FACE_OUTER_BOUND ( 'NONE', #11645, .T. ) ;
#7963=EDGE_LOOP ( 'NONE', ( #14229, #14785, #17793, #16406, #6957, #10111, #22202, #6350, #20456 ) ) ;
#7975=EDGE_CURVE ( 'NONE', #15056, #6828, #13772, .T. ) ;
#8039=VERTEX_POINT ( 'NONE', #21720 ) ;
#8079=EDGE_CURVE ( 'NONE', #15778, #18815, #6576, .T. ) ;
#8209=EDGE_CURVE ( 'NONE', #14761, #15790, #14897, .T. ) ;
#8211=CARTESIAN_POINT ( 'NONE',  ( 0.000000000000000000, -17.30000000000000071, -5.000000000000000000 ) ) ;
#8216=VERTEX_POINT ( 'NONE', #17905 ) ;
#8361=DIRECTION ( 'NONE',  ( 0.000000000000000000, -1.000000000000000000, 0.000000000000000000 ) ) ;
#8403=CARTESIAN_POINT ( 'NONE',  ( -16.50000000000000000, -20.00000000000000000, -5.000000000000000000 ) ) ;
#8421=VERTEX_POINT ( 'NONE', #21681 ) ;
#8425=CARTESIAN_POINT ( 'NONE',  ( 4.267766952966369765, -30.47499999999999787, -20.76776695296636888 ) ) ;
#8433=DIRECTION ( 'NONE',  ( 1.000000000000000000, 0.000000000000000000, 0.000000000000000000 ) ) ;
#8472=DIRECTION ( 'NONE',  ( 0.000000000000000000, 0.000000000000000000, 1.000000000000000000 ) ) ;
#8491=DIRECTION ( 'NONE',  ( 4.539762594625140272E-47, 1.000000000000000000, 0.000000000000000000 ) ) ;
#8498=VECTOR ( 'NONE', #1953, 1000.000000000000000 ) ;
#8512=CARTESIAN_POINT ( 'NONE',  ( -17.54011269262000283, -27.34999999999999787, -5.000000000000000000 ) ) ;
#8520=EDGE_CURVE ( 'NONE', #1171, #5066, #1853, .T. ) ;
#8636=CIRCLE ( 'NONE', #14359, 2.500000000000000000 ) ;
#8638=CARTESIAN_POINT ( 'NONE',  ( -11.00000000000000000, -27.34999999999999787, -6.250000000000000000 ) ) ;
#8653=CIRCLE ( 'NONE', #12457, 3.499999999999999556 ) ;
#8666=ORIENTED_EDGE ( 'NONE', *, *, #9214, .F. ) ;
#8674=ORIENTED_EDGE ( 'NONE', *, *, #15758, .F. ) ;
#8700=ORIENTED_EDGE ( 'NONE', *, *, #16450, .F. ) ;
#8743=ORIENTED_EDGE ( 'NONE', *, *, #12309, .F. ) ;
#8774=EDGE_LOOP ( 'NONE', ( #9345, #16507, #3064, #16861 ) ) ;
#8811=DIRECTION ( 'NONE',  ( 0.000000000000000000, 1.000000000000000000, 0.000000000000000000 ) ) ;
#8819=DIRECTION ( 'NONE',  ( 1.000000000000000000, 0.000000000000000000, 1.480297366166879989E-16 ) ) ;
#8857=VERTEX_POINT ( 'NONE', #19197 ) ;
#8866=DIRECTION ( 'NONE',  ( 0.000000000000000000, 0.000000000000000000, -1.000000000000000000 ) ) ;
#8889=ORIENTED_EDGE ( 'NONE', *, *, #12309, .T. ) ;
#8914=CARTESIAN_POINT ( 'NONE',  ( 0.000000000000000000, -17.30000000000000071, -2.500000000000000000 ) ) ;
#8930=ORIENTED_EDGE ( 'NONE', *, *, #10909, .F. ) ;
#8943=AXIS2_PLACEMENT_3D ( 'NONE', #19569, #14682, #1973 ) ;
#9013=CYLINDRICAL_SURFACE ( 'NONE', #5394, 2.500000000000000888 ) ;
#9019=EDGE_LOOP ( 'NONE', ( #16266, #2690, #17313, #2351 ) ) ;
#9029=DIRECTION ( 'NONE',  ( -1.000000000000000000, 0.000000000000000000, 0.000000000000000000 ) ) ;
#9035=EDGE_LOOP ( 'NONE', ( #14811, #22054, #1490, #1018 ) ) ;
#9041=DIRECTION ( 'NONE',  ( 0.000000000000000000, 0.000000000000000000, -1.000000000000000000 ) ) ;
#9063=DIRECTION ( 'NONE',  ( -1.000000000000000000, 0.000000000000000000, 0.000000000000000000 ) ) ;
#9083=DIRECTION ( 'NONE',  ( 0.000000000000000000, 0.000000000000000000, -1.000000000000000000 ) ) ;
#9127=DIRECTION ( 'NONE',  ( -0.7071067811865475727, 0.000000000000000000, -0.7071067811865475727 ) ) ;
#9131=EDGE_LOOP ( 'NONE', ( #21468, #8743, #21444, #7153 ) ) ;
#9214=EDGE_CURVE ( 'NONE', #1171, #7380, #18374, .T. ) ;
#9220=ORIENTED_EDGE ( 'NONE', *, *, #7641, .F. ) ;
#9229=AXIS2_PLACEMENT_3D ( 'NONE', #7479, #18528, #9029 ) ;
#9239=ORIENTED_EDGE ( 'NONE', *, *, #1084, .T. ) ;
#9277=CARTESIAN_POINT ( 'NONE',  ( 5.750000000000139444, -20.33108891324529921, -2.500000000000000000 ) ) ;
#9345=ORIENTED_EDGE ( 'NONE', *, *, #6017, .T. ) ;
#9351=CYLINDRICAL_SURFACE ( 'NONE', #10302, 2.500000000000000000 ) ;
#9435=FACE_OUTER_BOUND ( 'NONE', #9035, .T. ) ;
#9443=LINE ( 'NONE', #277, #11062 ) ;
#9460=DIRECTION ( 'NONE',  ( 0.000000000000000000, -1.000000000000000000, 0.000000000000000000 ) ) ;
#9473=FACE_OUTER_BOUND ( 'NONE', #5807, .T. ) ;
#9531=MANIFOLD_SOLID_BREP ( 'Boss-Extrude1', #17105 ) ;
#9541=ORIENTED_EDGE ( 'NONE', *, *, #3238, .T. ) ;
#9562=AXIS2_PLACEMENT_3D ( 'NONE', #17486, #8472, #21051 ) ;
#9740=CIRCLE ( 'NONE', #2510, 2.500000000000000000 ) ;
#9816=ADVANCED_FACE ( 'NONE', ( #15697 ), #22680, .T. ) ;
#9863=CYLINDRICAL_SURFACE ( 'NONE', #22516, 2.500000000000001332 ) ;
#9879=EDGE_CURVE ( 'NONE', #18433, #7459, #16325, .T. ) ;
#9887=ORIENTED_EDGE ( 'NONE', *, *, #13905, .F. ) ;
#9934=ORIENTED_EDGE ( 'NONE', *, *, #10562, .T. ) ;
#9993=VERTEX_POINT ( 'NONE', #13152 ) ;
#10021=CIRCLE ( 'NONE', #21754, 3.750000000000000000 ) ;
#10056=CYLINDRICAL_SURFACE ( 'NONE', #20184, 7.000000000000004441 ) ;
#10111=ORIENTED_EDGE ( 'NONE', *, *, #9214, .T. ) ;
#10141=ORIENTED_EDGE ( 'NONE', *, *, #13641, .F. ) ;
#10170=CARTESIAN_POINT ( 'NONE',  ( -27.00000000000000000, -20.00000000000000000, -2.500000000000000000 ) ) ;
#10175=CIRCLE ( 'NONE', #13195, 2.500000000000000000 ) ;
#10194=LINE ( 'NONE', #12331, #266 ) ;
#10222=DIRECTION ( 'NONE',  ( 0.000000000000000000, 0.000000000000000000, -1.000000000000000000 ) ) ;
#10247=EDGE_LOOP ( 'NONE', ( #13191, #22782, #5762, #2614, #19890, #18054, #8930, #6408 ) ) ;
#10253=DIRECTION ( 'NONE',  ( 1.000000000000000000, 0.000000000000000000, 1.480297366166879989E-16 ) ) ;
#10261=FACE_BOUND ( 'NONE', #15959, .T. ) ;
#10279=DIRECTION ( 'NONE',  ( 0.000000000000000000, 0.000000000000000000, -1.000000000000000000 ) ) ;
#10291=PLANE ( 'NONE',  #19076 ) ;
#10302=AXIS2_PLACEMENT_3D ( 'NONE', #1744, #18272, #7352 ) ;
#10359=ORIENTED_EDGE ( 'NONE', *, *, #15947, .T. ) ;
#10373=AXIS2_PLACEMENT_3D ( 'NONE', #7556, #15021, #11839 ) ;
#10407=FACE_OUTER_BOUND ( 'NONE', #10949, .T. ) ;
#10415=DIRECTION ( 'NONE',  ( 1.000000000000000000, -3.416070845000479880E-16, 0.000000000000000000 ) ) ;
#10441=DIRECTION ( 'NONE',  ( 0.000000000000000000, -1.000000000000000000, 0.000000000000000000 ) ) ;
#10449=VERTEX_POINT ( 'NONE', #10787 ) ;
#10456=ADVANCED_FACE ( 'NONE', ( #21900 ), #11132, .F. ) ;
#10546=VECTOR ( 'NONE', #9083, 1000.000000000000000 ) ;
#10562=EDGE_CURVE ( 'NONE', #15552, #2375, #9443, .T. ) ;
#10585=LINE ( 'NONE', #1519, #11526 ) ;
#10595=AXIS2_PLACEMENT_3D ( 'NONE', #8211, #13666, #1182 ) ;
#10660=EDGE_CURVE ( 'NONE', #20805, #13906, #7657, .T. ) ;
#10677=AXIS2_PLACEMENT_3D ( 'NONE', #11795, #19027, #3216 ) ;
#10679=CARTESIAN_POINT ( 'NONE',  ( 0.000000000000000000, 0.000000000000000000, -5.000000000000000000 ) ) ;
#10688=CARTESIAN_POINT ( 'NONE',  ( -4.514225866272970400, 4.676725866273559795, -2.500000000000000000 ) ) ;
#10722=CARTESIAN_POINT ( 'NONE',  ( 0.000000000000000000, -17.30000000000000071, -2.500000000000000000 ) ) ;
#10744=CIRCLE ( 'NONE', #12632, 2.500000000000000888 ) ;
#10762=EDGE_LOOP ( 'NONE', ( #6676, #19466, #17054, #8674 ) ) ;
#10787=CARTESIAN_POINT ( 'NONE',  ( 5.000000000000000000, -23.36217782649100272, -2.500000000000000000 ) ) ;
#10826=ADVANCED_FACE ( 'NONE', ( #10407 ), #15950, .F. ) ;
#10842=ORIENTED_EDGE ( 'NONE', *, *, #15496, .F. ) ;
#10878=DIRECTION ( 'NONE',  ( 0.000000000000000000, 0.000000000000000000, -1.000000000000000000 ) ) ;
#10891=DIRECTION ( 'NONE',  ( -1.000000000000000000, 0.000000000000000000, 0.000000000000000000 ) ) ;
#10909=EDGE_CURVE ( 'NONE', #10449, #8039, #16183, .T. ) ;
#10924=VECTOR ( 'NONE', #6555, 1000.000000000000000 ) ;
#10949=EDGE_LOOP ( 'NONE', ( #17573, #14666, #2726, #9887 ) ) ;
#10966=FACE_OUTER_BOUND ( 'NONE', #12922, .T. ) ;
#10999=LINE ( 'NONE', #3503, #6192 ) ;
#11034=CARTESIAN_POINT ( 'NONE',  ( 0.000000000000000000, -17.30000000000000071, -2.500000000000000000 ) ) ;
#11041=EDGE_CURVE ( 'NONE', #12652, #255, #2159, .T. ) ;
#11062=VECTOR ( 'NONE', #16662, 1000.000000000000000 ) ;
#11070=LINE ( 'NONE', #9277, #16303 ) ;
#11128=DIRECTION ( 'NONE',  ( 0.000000000000000000, 0.000000000000000000, 1.000000000000000000 ) ) ;
#11132=CYLINDRICAL_SURFACE ( 'NONE', #17113, 2.500000000000000000 ) ;
#11355=CARTESIAN_POINT ( 'NONE',  ( 0.000000000000000000, 0.000000000000000000, -2.500000000000000000 ) ) ;
#11384=DIRECTION ( 'NONE',  ( 0.000000000000000000, 0.000000000000000000, 1.000000000000000000 ) ) ;
#11402=AXIS2_PLACEMENT_3D ( 'NONE', #19136, #2733, #13651 ) ;
#11418=CARTESIAN_POINT ( 'NONE',  ( -27.00000000000000000, -20.00000000000000000, -5.000000000000000000 ) ) ;
#11426=CARTESIAN_POINT ( 'NONE',  ( 6.500000000000000000, 0.000000000000000000, -5.000000000000000000 ) ) ;
#11500=CARTESIAN_POINT ( 'NONE',  ( -26.26776695296636888, -28.60000000000000142, -20.76776695296636888 ) ) ;
#11526=VECTOR ( 'NONE', #17812, 1000.000000000000000 ) ;
#11543=ORIENTED_EDGE ( 'NONE', *, *, #13905, .T. ) ;
#11554=DIRECTION ( 'NONE',  ( 0.7071067811865475727, 0.000000000000000000, -0.7071067811865474617 ) ) ;
#11629=DIRECTION ( 'NONE',  ( -1.000000000000000000, 0.000000000000000000, 0.000000000000000000 ) ) ;
#11645=EDGE_LOOP ( 'NONE', ( #5862, #9541, #20655, #9934 ) ) ;
#11744=EDGE_LOOP ( 'NONE', ( #5241, #13168, #3576, #16844 ) ) ;
#11762=DIRECTION ( 'NONE',  ( -1.000000000000000000, 0.000000000000000000, 0.000000000000000000 ) ) ;
#11774=CIRCLE ( 'NONE', #14779, 6.500000000000000888 ) ;
#11777=CIRCLE ( 'NONE', #11402, 6.499999999999997335 ) ;
#11795=CARTESIAN_POINT ( 'NONE',  ( 2.500000000000000000, -30.47499999999999787, -19.00000000000000000 ) ) ;
#11811=DIRECTION ( 'NONE',  ( -0.7194962871189606313, -0.6944962871189667153, 0.000000000000000000 ) ) ;
#11837=VERTEX_POINT ( 'NONE', #18999 ) ;
#11839=DIRECTION ( 'NONE',  ( 0.7071067811865475727, 0.000000000000000000, -0.7071067811865474617 ) ) ;
#11963=FACE_OUTER_BOUND ( 'NONE', #17420, .T. ) ;
#11989=ORIENTED_EDGE ( 'NONE', *, *, #19575, .F. ) ;
#12010=DIRECTION ( 'NONE',  ( -2.972463603623604872E-47, -1.000000000000000000, -2.972463603623604872E-47 ) ) ;
#12063=CARTESIAN_POINT ( 'NONE',  ( 5.000000000000000000, -31.09999999999999787, -21.50000000000000000 ) ) ;
#12067=LINE ( 'NONE', #1099, #16373 ) ;
#12102=DIRECTION ( 'NONE',  ( 1.000000000000000000, 0.000000000000000000, 1.480297366166879989E-16 ) ) ;
#12144=LINE ( 'NONE', #15698, #10924 ) ;
#12224=DIRECTION ( 'NONE',  ( 0.000000000000000000, 0.000000000000000000, -1.000000000000000000 ) ) ;
#12232=DIRECTION ( 'NONE',  ( -1.000000000000000000, 0.000000000000000000, 0.000000000000000000 ) ) ;
#12233=CIRCLE ( 'NONE', #17526, 3.499999999999999556 ) ;
#12258=AXIS2_PLACEMENT_3D ( 'NONE', #6799, #10253, #3224 ) ;
#12290=VECTOR ( 'NONE', #1322, 1000.000000000000000 ) ;
#12309=EDGE_CURVE ( 'NONE', #6828, #15056, #8653, .T. ) ;
#12331=CARTESIAN_POINT ( 'NONE',  ( 6.500000000000000000, -17.30000000000000071, -5.000000000000000000 ) ) ;
#12335=CARTESIAN_POINT ( 'NONE',  ( -24.50000000000000000, -28.60000000000000142, -21.50000000000000000 ) ) ;
#12446=CARTESIAN_POINT ( 'NONE',  ( -27.00000000000000000, -20.00000000000000000, -2.500000000000000000 ) ) ;
#12457=AXIS2_PLACEMENT_3D ( 'NONE', #3377, #8866, #10891 ) ;
#12463=FACE_BOUND ( 'NONE', #3370, .T. ) ;
#12492=DIRECTION ( 'NONE',  ( 0.000000000000000000, -1.000000000000000000, 0.000000000000000000 ) ) ;
#12577=LINE ( 'NONE', #10688, #2917 ) ;
#12592=DIRECTION ( 'NONE',  ( 0.000000000000000000, 0.000000000000000000, -1.000000000000000000 ) ) ;
#12610=DIRECTION ( 'NONE',  ( -0.7071067811865475727, 0.000000000000000000, -0.7071067811865475727 ) ) ;
#12629=PLANE ( 'NONE',  #1902 ) ;
#12632=AXIS2_PLACEMENT_3D ( 'NONE', #18175, #12492, #12610 ) ;
#12652=VERTEX_POINT ( 'NONE', #978 ) ;
#12671=ORIENTED_EDGE ( 'NONE', *, *, #11041, .F. ) ;
#12705=CYLINDRICAL_SURFACE ( 'NONE', #22473, 3.499999999999999556 ) ;
#12739=AXIS2_PLACEMENT_3D ( 'NONE', #2569, #13380, #415 ) ;
#12785=PLANE ( 'NONE',  #7325 ) ;
#12787=AXIS2_PLACEMENT_3D ( 'NONE', #5774, #9460, #20621 ) ;
#12882=ADVANCED_FACE ( 'NONE', ( #6815 ), #21289, .F. ) ;
#12922=EDGE_LOOP ( 'NONE', ( #958, #19437, #5045, #18388 ) ) ;
#12959=VECTOR ( 'NONE', #4898, 1000.000000000000000 ) ;
#12974=CARTESIAN_POINT ( 'NONE',  ( 5.000000000000000000, -23.36217782649100272, -2.500000000000000000 ) ) ;
#13050=DIRECTION ( 'NONE',  ( 1.000000000000000000, 0.000000000000000000, 0.000000000000000000 ) ) ;
#13098=ORIENTED_EDGE ( 'NONE', *, *, #16450, .T. ) ;
#13129=LINE ( 'NONE', #528, #5797 ) ;
#13142=EDGE_CURVE ( 'NONE', #560, #6915, #21936, .T. ) ;
#13152=CARTESIAN_POINT ( 'NONE',  ( -24.50000000000000000, -31.09999999999999787, -21.50000000000000000 ) ) ;
#13167=DIRECTION ( 'NONE',  ( -2.312964634635742957E-16, 0.000000000000000000, 1.000000000000000000 ) ) ;
#13168=ORIENTED_EDGE ( 'NONE', *, *, #13751, .F. ) ;
#13178=VECTOR ( 'NONE', #22968, 1000.000000000000000 ) ;
#13185=ADVANCED_FACE ( 'NONE', ( #19024 ), #6549, .T. ) ;
#13191=ORIENTED_EDGE ( 'NONE', *, *, #19813, .T. ) ;
#13195=AXIS2_PLACEMENT_3D ( 'NONE', #43, #11128, #275 ) ;
#13240=DIRECTION ( 'NONE',  ( 0.000000000000000000, 0.000000000000000000, -1.000000000000000000 ) ) ;
#13242=DIRECTION ( 'NONE',  ( -0.6944962871189167553, 0.7194962871190087039, 0.000000000000000000 ) ) ;
#13247=ORIENTED_EDGE ( 'NONE', *, *, #4774, .F. ) ;
#13274=EDGE_LOOP ( 'NONE', ( #16688, #12671, #6632, #4430, #18066, #5442, #9239, #4746 ) ) ;
#13380=DIRECTION ( 'NONE',  ( 0.000000000000000000, 0.000000000000000000, 1.000000000000000000 ) ) ;
#13400=EDGE_LOOP ( 'NONE', ( #15674, #14383, #8666, #16506 ) ) ;
#13414=EDGE_CURVE ( 'NONE', #8216, #21157, #8636, .T. ) ;
#13477=LINE ( 'NONE', #22133, #15474 ) ;
#13543=CIRCLE ( 'NONE', #12787, 2.500000000000000888 ) ;
#13545=VECTOR ( 'NONE', #8491, 1000.000000000000000 ) ;
#13568=DIRECTION ( 'NONE',  ( 0.8846153846153640421, -0.4663213712685829182, 0.000000000000000000 ) ) ;
#13641=EDGE_CURVE ( 'NONE', #6915, #5066, #10194, .T. ) ;
#13647=CARTESIAN_POINT ( 'NONE',  ( -24.86147400983239919, -14.96352599016710094, -2.500000000000000000 ) ) ;
#13651=DIRECTION ( 'NONE',  ( 0.8846153846154072298, -0.4663213712685009837, 0.000000000000000000 ) ) ;
#13666=DIRECTION ( 'NONE',  ( 0.000000000000000000, 0.000000000000000000, 1.000000000000000000 ) ) ;
#13674=CARTESIAN_POINT ( 'NONE',  ( 5.000000000000000000, -28.60000000000000142, -6.250000000000000000 ) ) ;
#13682=ORIENTED_EDGE ( 'NONE', *, *, #6286, .F. ) ;
#13704=DIRECTION ( 'NONE',  ( 0.000000000000000000, 0.000000000000000000, -1.000000000000000000 ) ) ;
#13751=EDGE_CURVE ( 'NONE', #2375, #3635, #5279, .T. ) ;
#13752=VERTEX_POINT ( 'NONE', #16099 ) ;
#13760=EDGE_CURVE ( 'NONE', #15790, #14761, #10175, .T. ) ;
#13772=CIRCLE ( 'NONE', #9229, 3.499999999999999556 ) ;
#13780=VECTOR ( 'NONE', #10222, 1000.000000000000000 ) ;
#13798=CARTESIAN_POINT ( 'NONE',  ( -4.514225866272970400, 4.676725866273559795, -2.500000000000000000 ) ) ;
#13892=EDGE_CURVE ( 'NONE', #15778, #15790, #1830, .T. ) ;
#13905=EDGE_CURVE ( 'NONE', #18815, #14761, #7087, .T. ) ;
#13906=VERTEX_POINT ( 'NONE', #14556 ) ;
#13948=DIRECTION ( 'NONE',  ( -0.000000000000000000, 1.000000000000000000, 0.000000000000000000 ) ) ;
#13968=DESIGN_CONTEXT ( 'detailed design', #21439, 'design' ) ;
#13985=EDGE_CURVE ( 'NONE', #4748, #8216, #13477, .T. ) ;
#13986=AXIS2_PLACEMENT_3D ( 'NONE', #13798, #4409, #16994 ) ;
#14036=DIRECTION ( 'NONE',  ( 0.000000000000000000, 0.000000000000000000, 1.000000000000000000 ) ) ;
#14113=FACE_OUTER_BOUND ( 'NONE', #22228, .T. ) ;
#14166=DIRECTION ( 'NONE',  ( 0.000000000000000000, -1.000000000000000000, 0.000000000000000000 ) ) ;
#14214=VERTEX_POINT ( 'NONE', #1095 ) ;
#14216=EDGE_CURVE ( 'NONE', #13906, #12652, #15598, .T. ) ;
#14218=CARTESIAN_POINT ( 'NONE',  ( -2.500000000000000000, -17.30000000000000071, -2.500000000000000000 ) ) ;
#14229=ORIENTED_EDGE ( 'NONE', *, *, #5146, .T. ) ;
#14266=CARTESIAN_POINT ( 'NONE',  ( 5.000000000000000000, -31.09999999999999787, -21.50000000000000000 ) ) ;
#14287=ORIENTED_EDGE ( 'NONE', *, *, #792, .F. ) ;
#14293=CARTESIAN_POINT ( 'NONE',  ( -27.00000000000000000, -28.60000000000000142, -6.250000000000000000 ) ) ;
#14359=AXIS2_PLACEMENT_3D ( 'NONE', #4116, #11384, #11629 ) ;
#14368=ORIENTED_EDGE ( 'NONE', *, *, #13751, .T. ) ;
#14383=ORIENTED_EDGE ( 'NONE', *, *, #20521, .F. ) ;
#14407=FACE_OUTER_BOUND ( 'NONE', #22679, .T. ) ;
#14433=ORIENTED_EDGE ( 'NONE', *, *, #125, .F. ) ;
#14556=CARTESIAN_POINT ( 'NONE',  ( -27.00000000000000000, -31.09999999999999787, -19.00000000000000000 ) ) ;
#14595=CARTESIAN_POINT ( 'NONE',  ( -20.00000000000000000, -20.00000000000000000, -2.500000000000000000 ) ) ;
#14617=DIRECTION ( 'NONE',  ( -0.7071067811865475727, 0.000000000000000000, -0.7071067811865475727 ) ) ;
#14657=DIRECTION ( 'NONE',  ( 0.000000000000000000, 0.000000000000000000, 1.000000000000000000 ) ) ;
#14662=CARTESIAN_POINT ( 'NONE',  ( 2.500000000000000000, 3.061616997868383141E-16, -2.500000000000000000 ) ) ;
#14666=ORIENTED_EDGE ( 'NONE', *, *, #13892, .T. ) ;
#14682=DIRECTION ( 'NONE',  ( 0.000000000000000000, 0.000000000000000000, 1.000000000000000000 ) ) ;
#14722=LINE ( 'NONE', #13647, #13780 ) ;
#14740=EDGE_CURVE ( 'NONE', #577, #746, #12144, .T. ) ;
#14761=VERTEX_POINT ( 'NONE', #21037 ) ;
#14779=AXIS2_PLACEMENT_3D ( 'NONE', #22029, #22149, #6609 ) ;
#14785=ORIENTED_EDGE ( 'NONE', *, *, #20418, .T. ) ;
#14811=ORIENTED_EDGE ( 'NONE', *, *, #4041, .T. ) ;
#14886=DIRECTION ( 'NONE',  ( 1.000000000000000000, 0.000000000000000000, 1.480297366166879989E-16 ) ) ;
#14897=CIRCLE ( 'NONE', #17944, 2.500000000000000000 ) ;
#14933=DIRECTION ( 'NONE',  ( 0.000000000000000000, 0.000000000000000000, 1.000000000000000000 ) ) ;
#14942=DIRECTION ( 'NONE',  ( 1.000000000000000000, 0.000000000000000000, 1.480297366166879989E-16 ) ) ;
#14946=CARTESIAN_POINT ( 'NONE',  ( 5.000000000000000000, -27.34999999999999787, -6.250000000000000000 ) ) ;
#14963=ORIENTED_EDGE ( 'NONE', *, *, #10909, .T. ) ;
#15021=DIRECTION ( 'NONE',  ( 0.000000000000000000, 1.000000000000000000, 0.000000000000000000 ) ) ;
#15056=VERTEX_POINT ( 'NONE', #22304 ) ;
#15085=ORIENTED_EDGE ( 'NONE', *, *, #13641, .T. ) ;
#15182=PRODUCT ( 'F2', 'F2', '', ( #1709 ) ) ;
#15192=VERTEX_POINT ( 'NONE', #11418 ) ;
#15282=DIRECTION ( 'NONE',  ( 0.000000000000000000, 0.000000000000000000, -1.000000000000000000 ) ) ;
#15304=AXIS2_PLACEMENT_3D ( 'NONE', #23051, #5014, #14036 ) ;
#15342=DIRECTION ( 'NONE',  ( 0.000000000000000000, 0.000000000000000000, 1.000000000000000000 ) ) ;
#15370=ORIENTED_EDGE ( 'NONE', *, *, #19680, .F. ) ;
#15376=CARTESIAN_POINT ( 'NONE',  ( 5.000000000000000000, -31.09999999999999787, -2.500000000000000000 ) ) ;
#15474=VECTOR ( 'NONE', #22011, 1000.000000000000000 ) ;
#15485=DIRECTION ( 'NONE',  ( 0.000000000000000000, 0.000000000000000000, -1.000000000000000000 ) ) ;
#15490=LINE ( 'NONE', #10170, #3122 ) ;
#15496=EDGE_CURVE ( 'NONE', #21863, #8039, #6766, .T. ) ;
#15533=VERTEX_POINT ( 'NONE', #23006 ) ;
#15552=VERTEX_POINT ( 'NONE', #7117 ) ;
#15598=LINE ( 'NONE', #17502, #13545 ) ;
#15638=AXIS2_PLACEMENT_3D ( 'NONE', #84, #18514, #16359 ) ;
#15674=ORIENTED_EDGE ( 'NONE', *, *, #1239, .T. ) ;
#15697=FACE_OUTER_BOUND ( 'NONE', #9019, .T. ) ;
#15698=CARTESIAN_POINT ( 'NONE',  ( -26.26776695296636888, -30.47499999999999787, -20.76776695296636888 ) ) ;
#15758=EDGE_CURVE ( 'NONE', #6828, #7459, #12067, .T. ) ;
#15778=VERTEX_POINT ( 'NONE', #2902 ) ;
#15790=VERTEX_POINT ( 'NONE', #22841 ) ;
#15840=CARTESIAN_POINT ( 'NONE',  ( 5.000000000000000000, -28.60000000000000142, -2.500000000000000000 ) ) ;
#15857=EDGE_CURVE ( 'NONE', #16294, #14214, #19064, .T. ) ;
#15894=DIRECTION ( 'NONE',  ( -4.539762594625140272E-47, -1.000000000000000000, 0.000000000000000000 ) ) ;
#15947=EDGE_CURVE ( 'NONE', #7459, #18433, #12233, .T. ) ;
#15950=CYLINDRICAL_SURFACE ( 'NONE', #21884, 2.500000000000000000 ) ;
#15959=EDGE_LOOP ( 'NONE', ( #20500, #4709 ) ) ;
#15963=LINE ( 'NONE', #5269, #18874 ) ;
#15988=ORIENTED_EDGE ( 'NONE', *, *, #13985, .F. ) ;
#16007=DIRECTION ( 'NONE',  ( -2.972463603623604872E-47, -1.000000000000000000, -2.972463603623604872E-47 ) ) ;
#16022=CIRCLE ( 'NONE', #3514, 2.500000000000000888 ) ;
#16025=VECTOR ( 'NONE', #17642, 1000.000000000000000 ) ;
#16065=ADVANCED_FACE ( 'NONE', ( #21520 ), #2162, .F. ) ;
#16078=ORIENTED_EDGE ( 'NONE', *, *, #13760, .F. ) ;
#16099=CARTESIAN_POINT ( 'NONE',  ( 6.500000000000000000, -17.30000000000000071, -2.500000000000000000 ) ) ;
#16170=FACE_OUTER_BOUND ( 'NONE', #18366, .T. ) ;
#16183=LINE ( 'NONE', #12974, #641 ) ;
#16197=ORIENTED_EDGE ( 'NONE', *, *, #20493, .T. ) ;
#16266=ORIENTED_EDGE ( 'NONE', *, *, #3238, .F. ) ;
#16268=DIRECTION ( 'NONE',  ( 0.8846153846154072298, -0.4663213712685009837, 0.000000000000000000 ) ) ;
#16273=DIRECTION ( 'NONE',  ( 0.000000000000000000, 0.000000000000000000, 1.000000000000000000 ) ) ;
#16294=VERTEX_POINT ( 'NONE', #13674 ) ;
#16303=VECTOR ( 'NONE', #9041, 1000.000000000000000 ) ;
#16319=DIRECTION ( 'NONE',  ( 0.000000000000000000, 0.000000000000000000, -1.000000000000000000 ) ) ;
#16323=CARTESIAN_POINT ( 'NONE',  ( -16.50000000000000000, -20.00000000000000000, -2.500000000000000000 ) ) ;
#16325=CIRCLE ( 'NONE', #4199, 3.499999999999999556 ) ;
#16332=DIRECTION ( 'NONE',  ( 0.7071067811865475727, 0.000000000000000000, -0.7071067811865474617 ) ) ;
#16359=DIRECTION ( 'NONE',  ( 1.534091707905539846E-93, -1.630753928186650048E-31, 1.000000000000000000 ) ) ;
#16373=VECTOR ( 'NONE', #15485, 1000.000000000000000 ) ;
#16393=ORIENTED_EDGE ( 'NONE', *, *, #5138, .F. ) ;
#16406=ORIENTED_EDGE ( 'NONE', *, *, #5138, .T. ) ;
#16413=EDGE_CURVE ( 'NONE', #12652, #746, #10744, .T. ) ;
#16450=EDGE_CURVE ( 'NONE', #577, #13906, #16022, .T. ) ;
#16506=ORIENTED_EDGE ( 'NONE', *, *, #8520, .T. ) ;
#16507=ORIENTED_EDGE ( 'NONE', *, *, #16726, .F. ) ;
#16610=EDGE_LOOP ( 'NONE', ( #6608, #13098, #7863, #19481 ) ) ;
#16629=DIRECTION ( 'NONE',  ( 0.000000000000000000, 0.000000000000000000, -1.000000000000000000 ) ) ;
#16662=DIRECTION ( 'NONE',  ( 5.944927207247209745E-47, 1.000000000000000000, 0.000000000000000000 ) ) ;
#16663=VECTOR ( 'NONE', #1965, 1000.000000000000000 ) ;
#16673=FACE_OUTER_BOUND ( 'NONE', #5387, .T. ) ;
#16688=ORIENTED_EDGE ( 'NONE', *, *, #6286, .T. ) ;
#16726=EDGE_CURVE ( 'NONE', #20922, #18242, #14722, .T. ) ;
#16733=ORIENTED_EDGE ( 'NONE', *, *, #792, .T. ) ;
#16763=DIRECTION ( 'NONE',  ( 0.000000000000000000, 0.000000000000000000, -1.000000000000000000 ) ) ;
#16764=ORIENTED_EDGE ( 'NONE', *, *, #13892, .F. ) ;
#16783=DIRECTION ( 'NONE',  ( 1.000000000000000000, -3.416070845000479880E-16, 0.000000000000000000 ) ) ;
#16793=CARTESIAN_POINT ( 'NONE',  ( 0.000000000000000000, 2.220446049250309925E-15, -2.500000000000000000 ) ) ;
#16844=ORIENTED_EDGE ( 'NONE', *, *, #125, .T. ) ;
#16861=ORIENTED_EDGE ( 'NONE', *, *, #20521, .T. ) ;
#16896=CARTESIAN_POINT ( 'NONE',  ( -24.86147400983239919, -14.96352599016710094, -2.500000000000000000 ) ) ;
#16931=( LENGTH_UNIT ( ) NAMED_UNIT ( * ) SI_UNIT ( .MILLI., .METRE. ) );
#16937=EDGE_CURVE ( 'NONE', #3635, #9993, #23362, .T. ) ;
#16994=DIRECTION ( 'NONE',  ( 0.000000000000000000, 0.000000000000000000, 1.000000000000000000 ) ) ;
#17045=( NAMED_UNIT ( * ) SI_UNIT ( $, .STERADIAN. ) SOLID_ANGLE_UNIT ( ) );
#17054=ORIENTED_EDGE ( 'NONE', *, *, #15947, .F. ) ;
#17071=CIRCLE ( 'NONE', #20108, 2.500000000000000888 ) ;
#17105=CLOSED_SHELL ( 'NONE', ( #10826, #12882, #6970, #17782, #6453, #18138, #1651, #2665, #9816, #20595, #5799, #18103, #18535, #22483, #3266, #16065, #10456, #3324, #6004, #17464, #20249, #5650, #13185, #3992, #49 ) ) ;
#17113=AXIS2_PLACEMENT_3D ( 'NONE', #164, #7431, #7198 ) ;
#17122=CARTESIAN_POINT ( 'NONE',  ( -20.00000000000000000, -20.00000000000000000, -2.500000000000000000 ) ) ;
#17176=EDGE_CURVE ( 'NONE', #15056, #18433, #21789, .T. ) ;
#17209=AXIS2_PLACEMENT_3D ( 'NONE', #10722, #21604, #16268 ) ;
#17211=AXIS2_PLACEMENT_3D ( 'NONE', #8638, #12102, #19440 ) ;
#17313=ORIENTED_EDGE ( 'NONE', *, *, #7026, .T. ) ;
#17318=ORIENTED_EDGE ( 'NONE', *, *, #7412, .T. ) ;
#17396=DIRECTION ( 'NONE',  ( -1.000000000000000000, 0.000000000000000000, 0.000000000000000000 ) ) ;
#17420=EDGE_LOOP ( 'NONE', ( #22167, #212, #4891, #6920, #6986, #19044, #14368, #22173 ) ) ;
#17422=AXIS2_PLACEMENT_3D ( 'NONE', #21304, #1461, #10415 ) ;
#17451=VECTOR ( 'NONE', #8433, 1000.000000000000000 ) ;
#17464=ADVANCED_FACE ( 'NONE', ( #23278 ), #3449, .T. ) ;
#17486=CARTESIAN_POINT ( 'NONE',  ( -8.080225385240000335, -15.72171916155420313, -2.500000000000000000 ) ) ;
#17502=CARTESIAN_POINT ( 'NONE',  ( -27.00000000000000000, -30.47499999999999787, -19.00000000000000000 ) ) ;
#17518=FACE_OUTER_BOUND ( 'NONE', #13400, .T. ) ;
#17521=LINE ( 'NONE', #14293, #16025 ) ;
#17526=AXIS2_PLACEMENT_3D ( 'NONE', #18092, #7174, #9063 ) ;
#17573=ORIENTED_EDGE ( 'NONE', *, *, #8079, .F. ) ;
#17582=CARTESIAN_POINT ( 'NONE',  ( -24.50000000000000000, -31.09999999999999787, -19.00000000000000000 ) ) ;
#17642=DIRECTION ( 'NONE',  ( -1.000000000000000000, -1.829748171496159792E-16, -1.829748171496159792E-16 ) ) ;
#17669=FACE_OUTER_BOUND ( 'NONE', #4522, .T. ) ;
#17710=AXIS2_PLACEMENT_3D ( 'NONE', #12063, #13704, #8361 ) ;
#17782=ADVANCED_FACE ( 'NONE', ( #7959 ), #9863, .T. ) ;
#17791=DIRECTION ( 'NONE',  ( 0.000000000000000000, 0.000000000000000000, 1.000000000000000000 ) ) ;
#17793=ORIENTED_EDGE ( 'NONE', *, *, #21702, .T. ) ;
#17812=DIRECTION ( 'NONE',  ( -5.944927207247209745E-47, -1.000000000000000000, 0.000000000000000000 ) ) ;
#17905=CARTESIAN_POINT ( 'NONE',  ( 2.500000000000000000, -17.30000000000000071, -5.000000000000000000 ) ) ;
#17930=FACE_OUTER_BOUND ( 'NONE', #10762, .T. ) ;
#17944=AXIS2_PLACEMENT_3D ( 'NONE', #10679, #17791, #12232 ) ;
#18054=ORIENTED_EDGE ( 'NONE', *, *, #15496, .T. ) ;
#18065=CARTESIAN_POINT ( 'NONE',  ( -20.00000000000000000, -20.00000000000000000, -2.500000000000000000 ) ) ;
#18066=ORIENTED_EDGE ( 'NONE', *, *, #18119, .F. ) ;
#18092=CARTESIAN_POINT ( 'NONE',  ( -20.00000000000000000, -20.00000000000000000, -5.000000000000000000 ) ) ;
#18103=ADVANCED_FACE ( 'NONE', ( #3892 ), #18156, .T. ) ;
#18111=CARTESIAN_POINT ( 'NONE',  ( -4.514225866272970400, 4.676725866273559795, -2.500000000000000000 ) ) ;
#18119=EDGE_CURVE ( 'NONE', #18183, #20805, #10021, .T. ) ;
#18138=ADVANCED_FACE ( 'NONE', ( #3764 ), #9013, .T. ) ;
#18156=PLANE ( 'NONE',  #15638 ) ;
#18175=CARTESIAN_POINT ( 'NONE',  ( -24.50000000000000000, -28.60000000000000142, -19.00000000000000000 ) ) ;
#18183=VERTEX_POINT ( 'NONE', #195 ) ;
#18185=CYLINDRICAL_SURFACE ( 'NONE', #20619, 2.500000000000000888 ) ;
#18242=VERTEX_POINT ( 'NONE', #22527 ) ;
#18267=EDGE_LOOP ( 'NONE', ( #15988, #4495, #22767, #6688 ) ) ;
#18272=DIRECTION ( 'NONE',  ( 0.000000000000000000, 0.000000000000000000, -1.000000000000000000 ) ) ;
#18345=AXIS2_PLACEMENT_3D ( 'NONE', #23289, #7047, #19732 ) ;
#18349=CARTESIAN_POINT ( 'NONE',  ( 6.500000000000000000, 0.000000000000000000, -2.500000000000000000 ) ) ;
#18366=EDGE_LOOP ( 'NONE', ( #22809, #14433, #21706, #4345, #17318, #1862, #433, #8700 ) ) ;
#18368=ORIENTED_EDGE ( 'NONE', *, *, #4750, .F. ) ;
#18374=CIRCLE ( 'NONE', #20638, 6.500000000000000000 ) ;
#18388=ORIENTED_EDGE ( 'NONE', *, *, #16937, .T. ) ;
#18396=CARTESIAN_POINT ( 'NONE',  ( -24.50000000000000000, -30.47499999999999787, -19.00000000000000000 ) ) ;
#18401=EDGE_LOOP ( 'NONE', ( #6382, #20312 ) ) ;
#18433=VERTEX_POINT ( 'NONE', #8403 ) ;
#18514=DIRECTION ( 'NONE',  ( 1.000000000000000000, -5.944927207247209745E-47, -9.694713396002079468E-78 ) ) ;
#18528=DIRECTION ( 'NONE',  ( 0.000000000000000000, 0.000000000000000000, -1.000000000000000000 ) ) ;
#18535=ADVANCED_FACE ( 'NONE', ( #17669 ), #19206, .F. ) ;
#18580=CARTESIAN_POINT ( 'NONE',  ( 0.000000000000000000, 2.220446049250309925E-15, -5.000000000000000000 ) ) ;
#18583=AXIS2_PLACEMENT_3D ( 'NONE', #3609, #10878, #13568 ) ;
#18598=DIRECTION ( 'NONE',  ( 0.000000000000000000, 0.000000000000000000, -1.000000000000000000 ) ) ;
#18815=VERTEX_POINT ( 'NONE', #7663 ) ;
#18845=LINE ( 'NONE', #15376, #5055 ) ;
#18874=VECTOR ( 'NONE', #23196, 1000.000000000000000 ) ;
#18881=DIRECTION ( 'NONE',  ( 0.000000000000000000, 0.000000000000000000, -1.000000000000000000 ) ) ;
#18999=CARTESIAN_POINT ( 'NONE',  ( -27.00000000000000000, -27.34999999999999787, -5.000000000000000000 ) ) ;
#19017=EDGE_CURVE ( 'NONE', #544, #18183, #15490, .T. ) ;
#19024=FACE_OUTER_BOUND ( 'NONE', #8774, .T. ) ;
#19027=DIRECTION ( 'NONE',  ( -2.972463603623604872E-47, -1.000000000000000000, -2.972463603623604872E-47 ) ) ;
#19044=ORIENTED_EDGE ( 'NONE', *, *, #3676, .F. ) ;
#19056=AXIS2_PLACEMENT_3D ( 'NONE', #14946, #8819, #13167 ) ;
#19064=LINE ( 'NONE', #15840, #6917 ) ;
#19076=AXIS2_PLACEMENT_3D ( 'NONE', #1113, #19531, #19646 ) ;
#19136=CARTESIAN_POINT ( 'NONE',  ( 0.000000000000000000, -17.30000000000000071, -2.500000000000000000 ) ) ;
#19197=CARTESIAN_POINT ( 'NONE',  ( 4.267766952966368876, -31.09999999999999787, -20.76776695296636888 ) ) ;
#19206=CYLINDRICAL_SURFACE ( 'NONE', #17211, 1.250000000000000222 ) ;
#19226=ORIENTED_EDGE ( 'NONE', *, *, #7975, .T. ) ;
#19235=LINE ( 'NONE', #6660, #17451 ) ;
#19354=ORIENTED_EDGE ( 'NONE', *, *, #20053, .F. ) ;
#19411=DIRECTION ( 'NONE',  ( 0.000000000000000000, -1.000000000000000000, 0.000000000000000000 ) ) ;
#19437=ORIENTED_EDGE ( 'NONE', *, *, #14740, .T. ) ;
#19440=DIRECTION ( 'NONE',  ( 0.000000000000000000, 0.000000000000000000, 1.000000000000000000 ) ) ;
#19457=VECTOR ( 'NONE', #15894, 1000.000000000000000 ) ;
#19466=ORIENTED_EDGE ( 'NONE', *, *, #17176, .T. ) ;
#19481=ORIENTED_EDGE ( 'NONE', *, *, #16413, .T. ) ;
#19484=DIRECTION ( 'NONE',  ( -1.000000000000000000, 0.000000000000000000, 0.000000000000000000 ) ) ;
#19515=CARTESIAN_POINT ( 'NONE',  ( 0.000000000000000000, -17.30000000000000071, -2.500000000000000000 ) ) ;
#19531=DIRECTION ( 'NONE',  ( 1.000000000000000000, -4.539762594625140272E-47, -7.773397468430785553E-78 ) ) ;
#19546=DIRECTION ( 'NONE',  ( 0.000000000000000000, 1.000000000000000000, 0.000000000000000000 ) ) ;
#19569=CARTESIAN_POINT ( 'NONE',  ( 0.000000000000000000, -17.30000000000000071, -5.000000000000000000 ) ) ;
#19575=EDGE_CURVE ( 'NONE', #15192, #11837, #4666, .T. ) ;
#19625=VECTOR ( 'NONE', #16319, 1000.000000000000000 ) ;
#19646=DIRECTION ( 'NONE',  ( -1.534091707905539846E-93, -1.712291624595989929E-31, 1.000000000000000000 ) ) ;
#19675=LINE ( 'NONE', #14218, #21335 ) ;
#19680=EDGE_CURVE ( 'NONE', #18242, #15192, #6983, .T. ) ;
#19692=FACE_BOUND ( 'NONE', #18401, .T. ) ;
#19732=DIRECTION ( 'NONE',  ( -0.6944962871189167553, 0.7194962871190087039, 0.000000000000000000 ) ) ;
#19813=EDGE_CURVE ( 'NONE', #22408, #8421, #20570, .T. ) ;
#19835=AXIS2_PLACEMENT_3D ( 'NONE', #6279, #18881, #11762 ) ;
#19861=CIRCLE ( 'NONE', #6973, 2.500000000000000000 ) ;
#19887=CYLINDRICAL_SURFACE ( 'NONE', #18583, 6.500000000000000888 ) ;
#19890=ORIENTED_EDGE ( 'NONE', *, *, #4722, .F. ) ;
#19907=EDGE_LOOP ( 'NONE', ( #8889, #19226 ) ) ;
#19918=CARTESIAN_POINT ( 'NONE',  ( 5.750000000000139444, -20.33108891324529921, -5.000000000000000000 ) ) ;
#19940=DIRECTION ( 'NONE',  ( -1.000000000000000000, 0.000000000000000000, 0.000000000000000000 ) ) ;
#19996=DIRECTION ( 'NONE',  ( 0.000000000000000000, 0.000000000000000000, 1.000000000000000000 ) ) ;
#20042=CARTESIAN_POINT ( 'NONE',  ( -27.00000000000000000, -27.34999999999999787, -6.250000000000000000 ) ) ;
#20053=EDGE_CURVE ( 'NONE', #15533, #21157, #19675, .T. ) ;
#20108=AXIS2_PLACEMENT_3D ( 'NONE', #17582, #22664, #6409 ) ;
#20184=AXIS2_PLACEMENT_3D ( 'NONE', #20715, #18598, #13242 ) ;
#20196=ORIENTED_EDGE ( 'NONE', *, *, #22161, .F. ) ;
#20205=CARTESIAN_POINT ( 'NONE',  ( -24.50000000000000000, -30.47499999999999787, -19.00000000000000000 ) ) ;
#20224=DIRECTION ( 'NONE',  ( 0.000000000000000000, 0.000000000000000000, -1.000000000000000000 ) ) ;
#20234=VERTEX_POINT ( 'NONE', #7333 ) ;
#20249=ADVANCED_FACE ( 'NONE', ( #16673 ), #12785, .T. ) ;
#20273=DIRECTION ( 'NONE',  ( 0.7071067811865475727, 0.000000000000000000, -0.7071067811865474617 ) ) ;
#20301=EDGE_CURVE ( 'NONE', #20234, #14214, #1235, .T. ) ;
#20302=EDGE_CURVE ( 'NONE', #2200, #8857, #4657, .T. ) ;
#20312=ORIENTED_EDGE ( 'NONE', *, *, #13414, .T. ) ;
#20356=AXIS2_PLACEMENT_3D ( 'NONE', #7118, #5661, #13050 ) ;
#20418=EDGE_CURVE ( 'NONE', #22408, #10449, #18845, .T. ) ;
#20437=CARTESIAN_POINT ( 'NONE',  ( 5.750000000000139444, -20.33108891324529921, -2.500000000000000000 ) ) ;
#20456=ORIENTED_EDGE ( 'NONE', *, *, #19017, .T. ) ;
#20458=ORIENTED_EDGE ( 'NONE', *, *, #1239, .F. ) ;
#20493=EDGE_CURVE ( 'NONE', #16294, #255, #17521, .T. ) ;
#20500=ORIENTED_EDGE ( 'NONE', *, *, #2097, .T. ) ;
#20521=EDGE_CURVE ( 'NONE', #7380, #2028, #5052, .T. ) ;
#20560=DIRECTION ( 'NONE',  ( -1.000000000000000000, 0.000000000000000000, 0.000000000000000000 ) ) ;
#20570=CIRCLE ( 'NONE', #19056, 3.750000000000000000 ) ;
#20571=AXIS2_PLACEMENT_3D ( 'NONE', #3170, #10441, #22981 ) ;
#20577=ORIENTED_EDGE ( 'NONE', *, *, #8079, .T. ) ;
#20595=ADVANCED_FACE ( 'NONE', ( #21186 ), #10291, .F. ) ;
#20618=LINE ( 'NONE', #539, #16663 ) ;
#20619=AXIS2_PLACEMENT_3D ( 'NONE', #20205, #21850, #3933 ) ;
#20621=DIRECTION ( 'NONE',  ( -0.7071067811865475727, 0.000000000000000000, -0.7071067811865475727 ) ) ;
#20638=AXIS2_PLACEMENT_3D ( 'NONE', #16793, #520, #7775 ) ;
#20655=ORIENTED_EDGE ( 'NONE', *, *, #23468, .T. ) ;
#20693=EDGE_LOOP ( 'NONE', ( #10359, #377 ) ) ;
#20701=CIRCLE ( 'NONE', #581, 2.500000000000001332 ) ;
#20715=CARTESIAN_POINT ( 'NONE',  ( -20.00000000000000000, -20.00000000000000000, -2.500000000000000000 ) ) ;
#20739=DIRECTION ( 'NONE',  ( 0.8846153846153640421, -0.4663213712685829182, 0.000000000000000000 ) ) ;
#20805=VERTEX_POINT ( 'NONE', #728 ) ;
#20808=CARTESIAN_POINT ( 'NONE',  ( -4.514225866272970400, 4.676725866273559795, -5.000000000000000000 ) ) ;
#20819=PRODUCT_DEFINITION ( 'UNKNOWN', '', #6956, #13968 ) ;
#20827=FACE_OUTER_BOUND ( 'NONE', #11744, .T. ) ;
#20837=VECTOR ( 'NONE', #11811, 999.9999999999998863 ) ;
#20862=ORIENTED_EDGE ( 'NONE', *, *, #6017, .F. ) ;
#20922=VERTEX_POINT ( 'NONE', #16896 ) ;
#21017=CARTESIAN_POINT ( 'NONE',  ( 2.500000000000000000, -30.47499999999999787, -19.00000000000000000 ) ) ;
#21037=CARTESIAN_POINT ( 'NONE',  ( -2.500000000000000000, 0.000000000000000000, -5.000000000000000000 ) ) ;
#21051=DIRECTION ( 'NONE',  ( 1.000000000000000000, 0.000000000000000000, 0.000000000000000000 ) ) ;
#21157=VERTEX_POINT ( 'NONE', #5364 ) ;
#21184=DIRECTION ( 'NONE',  ( 1.000000000000000000, 0.000000000000000000, 0.000000000000000000 ) ) ;
#21186=FACE_OUTER_BOUND ( 'NONE', #13274, .T. ) ;
#21289=CYLINDRICAL_SURFACE ( 'NONE', #4101, 2.500000000000000000 ) ;
#21304=CARTESIAN_POINT ( 'NONE',  ( 0.000000000000000000, 2.220446049250309925E-15, -2.500000000000000000 ) ) ;
#21306=DIRECTION ( 'NONE',  ( 0.000000000000000000, 0.000000000000000000, -1.000000000000000000 ) ) ;
#21335=VECTOR ( 'NONE', #12224, 1000.000000000000000 ) ;
#21359=DIRECTION ( 'NONE',  ( -0.7194962871189606313, -0.6944962871189667153, 0.000000000000000000 ) ) ;
#21401=LINE ( 'NONE', #2992, #12959 ) ;
#21405=DIRECTION ( 'NONE',  ( 0.000000000000000000, 0.000000000000000000, -1.000000000000000000 ) ) ;
#21439=APPLICATION_CONTEXT ( 'configuration controlled 3d designs of mechanical parts and assemblies' ) ;
#21444=ORIENTED_EDGE ( 'NONE', *, *, #15758, .T. ) ;
#21465=EDGE_CURVE ( 'NONE', #4748, #15533, #2123, .T. ) ;
#21466=CARTESIAN_POINT ( 'NONE',  ( 5.000000000000000000, -31.09999999999999787, -5.000000000000000000 ) ) ;
#21468=ORIENTED_EDGE ( 'NONE', *, *, #17176, .F. ) ;
#21520=FACE_OUTER_BOUND ( 'NONE', #9131, .T. ) ;
#21553=ORIENTED_EDGE ( 'NONE', *, *, #816, .T. ) ;
#21590=CARTESIAN_POINT ( 'NONE',  ( -4.514225866272970400, 4.676725866273559795, -5.000000000000000000 ) ) ;
#21604=DIRECTION ( 'NONE',  ( 0.000000000000000000, 0.000000000000000000, -1.000000000000000000 ) ) ;
#21626=ORIENTED_EDGE ( 'NONE', *, *, #8209, .T. ) ;
#21676=CARTESIAN_POINT ( 'NONE',  ( -26.26776695296636888, -31.09999999999999787, -20.76776695296636888 ) ) ;
#21681=CARTESIAN_POINT ( 'NONE',  ( 5.000000000000000000, -31.09999999999999787, -6.250000000000000000 ) ) ;
#21688=CIRCLE ( 'NONE', #20571, 2.500000000000001332 ) ;
#21702=EDGE_CURVE ( 'NONE', #10449, #418, #4440, .T. ) ;
#21706=ORIENTED_EDGE ( 'NONE', *, *, #23468, .F. ) ;
#21720=CARTESIAN_POINT ( 'NONE',  ( 5.000000000000000000, -23.36217782649100272, -5.000000000000000000 ) ) ;
#21750=VECTOR ( 'NONE', #22035, 1000.000000000000000 ) ;
#21754=AXIS2_PLACEMENT_3D ( 'NONE', #20042, #14942, #22169 ) ;
#21789=LINE ( 'NONE', #16323, #8498 ) ;
#21798=CARTESIAN_POINT ( 'NONE',  ( 6.500000000000000000, -17.30000000000000071, -2.500000000000000000 ) ) ;
#21806=ADVANCED_BREP_SHAPE_REPRESENTATION ( '', ( #9531, #12739 ), #2093 ) ;
#21828=CARTESIAN_POINT ( 'NONE',  ( 5.000000000000000000, -31.09999999999999787, -19.00000000000000000 ) ) ;
#21850=DIRECTION ( 'NONE',  ( 2.269881297312570136E-47, 1.000000000000000000, -2.269881297312570136E-47 ) ) ;
#21863=VERTEX_POINT ( 'NONE', #23218 ) ;
#21884=AXIS2_PLACEMENT_3D ( 'NONE', #23066, #10279, #17396 ) ;
#21900=FACE_OUTER_BOUND ( 'NONE', #18267, .T. ) ;
#21936=CIRCLE ( 'NONE', #10595, 6.499999999999997335 ) ;
#22011=DIRECTION ( 'NONE',  ( 0.000000000000000000, 0.000000000000000000, -1.000000000000000000 ) ) ;
#22019=EDGE_CURVE ( 'NONE', #746, #3635, #13543, .T. ) ;
#22029=CARTESIAN_POINT ( 'NONE',  ( 11.50000000000000000, -23.36217782649110219, -5.000000000000000000 ) ) ;
#22035=DIRECTION ( 'NONE',  ( 0.000000000000000000, 0.000000000000000000, -1.000000000000000000 ) ) ;
#22054=ORIENTED_EDGE ( 'NONE', *, *, #19813, .F. ) ;
#22119=LINE ( 'NONE', #20808, #20837 ) ;
#22133=CARTESIAN_POINT ( 'NONE',  ( 2.500000000000000000, -17.30000000000000071, -2.500000000000000000 ) ) ;
#22149=DIRECTION ( 'NONE',  ( 0.000000000000000000, 0.000000000000000000, -1.000000000000000000 ) ) ;
#22154=( NAMED_UNIT ( * ) PLANE_ANGLE_UNIT ( ) SI_UNIT ( $, .RADIAN. ) );
#22161=EDGE_CURVE ( 'NONE', #21863, #11837, #1238, .T. ) ;
#22167=ORIENTED_EDGE ( 'NONE', *, *, #16413, .F. ) ;
#22169=DIRECTION ( 'NONE',  ( 0.000000000000000000, 0.000000000000000000, 1.000000000000000000 ) ) ;
#22173=ORIENTED_EDGE ( 'NONE', *, *, #22019, .F. ) ;
#22202=ORIENTED_EDGE ( 'NONE', *, *, #3188, .T. ) ;
#22218=DIRECTION ( 'NONE',  ( -1.000000000000000000, 0.000000000000000000, 0.000000000000000000 ) ) ;
#22225=ORIENTED_EDGE ( 'NONE', *, *, #13760, .T. ) ;
#22228=EDGE_LOOP ( 'NONE', ( #7417, #11989, #15370, #20862, #20458, #10141, #22632, #4029, #10842 ) ) ;
#22233=CYLINDRICAL_SURFACE ( 'NONE', #267, 3.750000000000000000 ) ;
#22235=DIRECTION ( 'NONE',  ( 0.000000000000000000, 0.000000000000000000, -1.000000000000000000 ) ) ;
#22304=CARTESIAN_POINT ( 'NONE',  ( -16.50000000000000000, -20.00000000000000000, -2.500000000000000000 ) ) ;
#22368=ORIENTED_EDGE ( 'NONE', *, *, #16726, .T. ) ;
#22408=VERTEX_POINT ( 'NONE', #7883 ) ;
#22473=AXIS2_PLACEMENT_3D ( 'NONE', #14595, #12592, #19940 ) ;
#22483=ADVANCED_FACE ( 'NONE', ( #9435 ), #22233, .T. ) ;
#22516=AXIS2_PLACEMENT_3D ( 'NONE', #21017, #12010, #11554 ) ;
#22527=CARTESIAN_POINT ( 'NONE',  ( -24.86147400983239919, -14.96352599016710094, -5.000000000000000000 ) ) ;
#22632=ORIENTED_EDGE ( 'NONE', *, *, #13142, .F. ) ;
#22664=DIRECTION ( 'NONE',  ( 0.000000000000000000, 1.000000000000000000, 0.000000000000000000 ) ) ;
#22679=EDGE_LOOP ( 'NONE', ( #21553, #13247, #7952, #14963 ) ) ;
#22680=CYLINDRICAL_SURFACE ( 'NONE', #10677, 2.500000000000001332 ) ;
#22767=ORIENTED_EDGE ( 'NONE', *, *, #20053, .T. ) ;
#22782=ORIENTED_EDGE ( 'NONE', *, *, #7412, .F. ) ;
#22809=ORIENTED_EDGE ( 'NONE', *, *, #5201, .F. ) ;
#22841=CARTESIAN_POINT ( 'NONE',  ( 2.500000000000000000, 3.061616997868383141E-16, -5.000000000000000000 ) ) ;
#22903=FACE_BOUND ( 'NONE', #20693, .T. ) ;
#22962=PLANE ( 'NONE',  #4905 ) ;
#22964=CARTESIAN_POINT ( 'NONE',  ( -4.514225866272970400, 4.676725866273559795, -2.500000000000000000 ) ) ;
#22968=DIRECTION ( 'NONE',  ( -1.000000000000000000, 0.000000000000000000, 0.000000000000000000 ) ) ;
#22981=DIRECTION ( 'NONE',  ( 0.7071067811865475727, 0.000000000000000000, -0.7071067811865474617 ) ) ;
#23006=CARTESIAN_POINT ( 'NONE',  ( -2.500000000000000000, -17.30000000000000071, -2.500000000000000000 ) ) ;
#23044=CARTESIAN_POINT ( 'NONE',  ( 2.500000000000000000, -17.30000000000000071, -2.500000000000000000 ) ) ;
#23051=CARTESIAN_POINT ( 'NONE',  ( -27.00000000000000000, -27.34999999999999787, -6.250000000000000000 ) ) ;
#23066=CARTESIAN_POINT ( 'NONE',  ( 0.000000000000000000, 0.000000000000000000, -2.500000000000000000 ) ) ;
#23196=DIRECTION ( 'NONE',  ( 0.000000000000000000, 0.000000000000000000, -1.000000000000000000 ) ) ;
#23207=AXIS2_PLACEMENT_3D ( 'NONE', #18065, #16273, #4606 ) ;
#23218=CARTESIAN_POINT ( 'NONE',  ( 5.000000000000000000, -27.34999999999999787, -5.000000000000000000 ) ) ;
#23278=FACE_OUTER_BOUND ( 'NONE', #3765, .T. ) ;
#23289=CARTESIAN_POINT ( 'NONE',  ( -20.00000000000000000, -20.00000000000000000, -5.000000000000000000 ) ) ;
#23291=FACE_BOUND ( 'NONE', #19907, .T. ) ;
#23303=EDGE_CURVE ( 'NONE', #21157, #8216, #6276, .T. ) ;
#23356=PLANE ( 'NONE',  #20356 ) ;
#23362=LINE ( 'NONE', #1399, #19457 ) ;
#23445=CARTESIAN_POINT ( 'NONE',  ( 2.500000000000000000, -28.60000000000000142, -21.50000000000000000 ) ) ;
#23468=EDGE_CURVE ( 'NONE', #8857, #15552, #20701, .T. ) ;
#23522=COLOUR_RGB('Light Blue', 0.66274510, 0.83137255, 0.94901961);
#23523=FILL_AREA_STYLE_COLOUR('',#23522);
#23524=FILL_AREA_STYLE('',(#23523));
#23525=SURFACE_STYLE_FILL_AREA(#23524);
#23526=SURFACE_SIDE_STYLE('',(#23525));
#23527=SURFACE_STYLE_USAGE(.BOTH.,#23526);
#23528=PRESENTATION_STYLE_ASSIGNMENT((#23527));
#23625=STYLED_ITEM('',(#23528),#9531);
#23626=MECHANICAL_DESIGN_GEOMETRIC_PRESENTATION_REPRESENTATION('',(#23625),#2093);
ENDSEC;
END-ISO-10303-21;
